ISO-10303-21;
HEADER;
FILE_DESCRIPTION (('STEP AP214'),
    '1' );
FILE_NAME ('hex nut style 1_am_B18.2.4.1M - Hex nut, Style 1,  M10 x 1.5, with 16mm WAF --D-N__PD3118.step',
    '2026-10-24T15:53:57',
    ( '' ),
    ( '' ),
    'SwSTEP 2.0',
    'SolidWorks 2025',
    '' );
FILE_SCHEMA (( 'AUTOMOTIVE_DESIGN' ));
ENDSEC;

DATA;
#3=FACE_BOUND ( 'NONE', #2659, .T. ) ;
#28=CARTESIAN_POINT ( 'NONE',  ( -0.6527133886630764881, 8.860760056385830197, -0.4969600502618033433 ) ) ;
#55=CARTESIAN_POINT ( 'NONE',  ( -8.000000000000225597, 0.7809653281575857919, -1.307852751878529391E-13 ) ) ;
#57=AXIS2_PLACEMENT_3D ( 'NONE', #6154, #7965, #2782 ) ;
#62=ADVANCED_FACE ( 'NONE', ( #7235 ), #7793, .T. ) ;
#67=CARTESIAN_POINT ( 'NONE',  ( 4.000000000000003553, -6.928203230275542523, -8.400000000000018119 ) ) ;
#76=CARTESIAN_POINT ( 'NONE',  ( 0.000000000000000000, 0.000000000000000000, -8.400000000000018119 ) ) ;
#80=EDGE_CURVE ( 'NONE', #838, #2390, #1314, .T. ) ;
#93=DIRECTION ( 'NONE',  ( 0.5000000000000035527, 0.8660254037844365982, 0.000000000000000000 ) ) ;
#101=DIRECTION ( 'NONE',  ( 1.000000000000000000, 8.881784197001244435E-16, 0.000000000000000000 ) ) ;
#103=CARTESIAN_POINT ( 'NONE',  ( -3.999999999999781508, -6.928203230275875590, 0.000000000000000000 ) ) ;
#106=AXIS2_PLACEMENT_3D ( 'NONE', #6926, #4870, #7530 ) ;
#118=CARTESIAN_POINT ( 'NONE',  ( -6.661338147750939243E-13, -9.237604307034352757, -0.7145311798163467287 ) ) ;
#121=AXIS2_PLACEMENT_3D ( 'NONE', #7183, #2433, #3907 ) ;
#126=AXIS2_PLACEMENT_3D ( 'NONE', #3777, #2508, #508 ) ;
#152=CARTESIAN_POINT ( 'NONE',  ( -5.690023276062281532, -5.952467836904624221, -0.1306530452039605383 ) ) ;
#190=CARTESIAN_POINT ( 'NONE',  ( 0.000000000000000000, 9.237604307034130713, -7.685468820183672278 ) ) ;
#192=DIRECTION ( 'NONE',  ( -1.000000000000000000, -8.881784197001244435E-16, -0.000000000000000000 ) ) ;
#205=CONICAL_SURFACE ( 'NONE', #4669, 8.000000000000007105, 1.047197551196597631 ) ;
#210=ORIENTED_EDGE ( 'NONE', *, *, #6998, .T. ) ;
#247=CARTESIAN_POINT ( 'NONE',  ( 8.000000000000229150, -4.440892098500626162E-13, 0.000000000000000000 ) ) ;
#258=ORIENTED_EDGE ( 'NONE', *, *, #80, .F. ) ;
#274=CIRCLE ( 'NONE', #551, 8.000000000000007105 ) ;
#280=AXIS2_PLACEMENT_3D ( 'NONE', #7220, #2059, #7465 ) ;
#286=EDGE_LOOP ( 'NONE', ( #851, #3513, #5956 ) ) ;
#294=CARTESIAN_POINT ( 'NONE',  ( -6.661338147750939243E-13, -9.237604307034352757, -0.7145311798163467287 ) ) ;
#338=FACE_OUTER_BOUND ( 'NONE', #5605, .T. ) ;
#345=DIRECTION ( 'NONE',  ( 0.000000000000000000, 0.000000000000000000, 1.000000000000000000 ) ) ;
#362=ADVANCED_FACE ( 'NONE', ( #2551 ), #3698, .F. ) ;
#387=DIRECTION ( 'NONE',  ( 0.000000000000000000, 0.000000000000000000, 1.000000000000000000 ) ) ;
#398=VECTOR ( 'NONE', #4921, 1000.000000000000000 ) ;
#401=B_SPLINE_CURVE_WITH_KNOTS ( 'NONE', 3,
 ( #1259, #743, #8059, #702, #2750, #2709 ),
 .UNSPECIFIED., .F., .F.,
 ( 4, 2, 4 ),
 ( 0.008240550023493506751, 0.01057684187039422546, 0.01291313371729494418 ),
 .UNSPECIFIED. ) ;
#405=ORIENTED_EDGE ( 'NONE', *, *, #3410, .F. ) ;
#435=ORIENTED_EDGE ( 'NONE', *, *, #2401, .T. ) ;
#452=EDGE_CURVE ( 'NONE', #3139, #799, #6073, .T. ) ;
#475=LINE ( 'NONE', #5807, #2024 ) ;
#478=ORIENTED_EDGE ( 'NONE', *, *, #4857, .F. ) ;
#497=DIRECTION ( 'NONE',  ( -1.000000000000000000, -8.881784197001244435E-16, 0.000000000000000000 ) ) ;
#503=CARTESIAN_POINT ( 'NONE',  ( 3.999999999999559464, 6.928203230274987412, -8.400000000000018119 ) ) ;
#508=DIRECTION ( 'NONE',  ( -1.000000000000000000, -8.881784197001244435E-16, 0.000000000000000000 ) ) ;
#531=CIRCLE ( 'NONE', #121, 8.000000000000007105 ) ;
#549=ORIENTED_EDGE ( 'NONE', *, *, #1644, .T. ) ;
#551=AXIS2_PLACEMENT_3D ( 'NONE', #7520, #6310, #6955 ) ;
#553=CARTESIAN_POINT ( 'NONE',  ( 0.6543471694410692985, 8.859816792613512959, -0.4964154566687120074 ) ) ;
#555=ORIENTED_EDGE ( 'NONE', *, *, #3272, .T. ) ;
#568=CARTESIAN_POINT ( 'NONE',  ( 0.000000000000000000, 0.000000000000000000, -8.400000000000018119 ) ) ;
#569=VERTEX_POINT ( 'NONE', #6106 ) ;
#582=CARTESIAN_POINT ( 'NONE',  ( 0.6543471694410680772, 8.859816792613512959, -7.903584543331305667 ) ) ;
#596=ORIENTED_EDGE ( 'NONE', *, *, #7934, .T. ) ;
#601=CARTESIAN_POINT ( 'NONE',  ( -8.000000000000220268, -1.555946510856261567, -0.06708870216349256677 ) ) ;
#610=B_SPLINE_CURVE_WITH_KNOTS ( 'NONE', 3,
 ( #103, #7440, #820, #1470, #152, #5802, #5108, #3694 ),
 .UNSPECIFIED., .F., .F.,
 ( 4, 2, 2, 4 ),
 ( 0.004673709593151774075, 0.005837709341827349366, 0.007001709090502924657, 0.009329708587854076973 ),
 .UNSPECIFIED. ) ;
#612=ORIENTED_EDGE ( 'NONE', *, *, #2401, .F. ) ;
#625=CARTESIAN_POINT ( 'NONE',  ( -8.000000000000007105, 0.000000000000000000, 0.000000000000000000 ) ) ;
#641=DIRECTION ( 'NONE',  ( 0.000000000000000000, 0.000000000000000000, 1.000000000000000000 ) ) ;
#648=FACE_OUTER_BOUND ( 'NONE', #286, .T. ) ;
#649=CARTESIAN_POINT ( 'NONE',  ( -6.686525924292996415, 5.377136764700138016, -8.083279549040094381 ) ) ;
#674=FACE_OUTER_BOUND ( 'NONE', #7400, .T. ) ;
#680=DIRECTION ( 'NONE',  ( 0.000000000000000000, 0.000000000000000000, -1.000000000000000000 ) ) ;
#702=CARTESIAN_POINT ( 'NONE',  ( -8.000000000000220268, -1.555946510856260012, -8.332911297836524511 ) ) ;
#705=B_SPLINE_CURVE_WITH_KNOTS ( 'NONE', 3,
 ( #1623, #2857, #7561, #4159, #4251, #6265, #2939, #2287 ),
 .UNSPECIFIED., .F., .F.,
 ( 4, 2, 2, 4 ),
 ( 0.004673709593151987446, 0.005837709341827518501, 0.007001709090503049557, 0.009329708587854111668 ),
 .UNSPECIFIED. ) ;
#722=CARTESIAN_POINT ( 'NONE',  ( 8.000000000000008882, 1.572549600175326745, -8.331055444744915661 ) ) ;
#734=CARTESIAN_POINT ( 'NONE',  ( -3.660532965669041516, 7.124194613927598674, -8.399999999999977263 ) ) ;
#735=CARTESIAN_POINT ( 'NONE',  ( -8.000000000000229150, 3.871967595402046491, -7.901061386767464612 ) ) ;
#743=CARTESIAN_POINT ( 'NONE',  ( -8.000000000000222045, -3.867591403079426282, -7.902324684675259725 ) ) ;
#756=CARTESIAN_POINT ( 'NONE',  ( 0.000000000000000000, 0.000000000000000000, 0.000000000000000000 ) ) ;
#773=FACE_OUTER_BOUND ( 'NONE', #7131, .T. ) ;
#783=ORIENTED_EDGE ( 'NONE', *, *, #3254, .T. ) ;
#794=ORIENTED_EDGE ( 'NONE', *, *, #2912, .F. ) ;
#799=VERTEX_POINT ( 'NONE', #8449 ) ;
#808=CARTESIAN_POINT ( 'NONE',  ( 4.681481898396925523, -6.534749472788245583, -8.399999999999996803 ) ) ;
#810=CARTESIAN_POINT ( 'NONE',  ( 7.999999999999563016, -4.618802153517398423, -0.7145311798163467287 ) ) ;
#815=B_SPLINE_CURVE_WITH_KNOTS ( 'NONE', 3,
 ( #1481, #3403, #3353, #6766, #6964, #7357 ),
 .UNSPECIFIED., .F., .F.,
 ( 4, 2, 4 ),
 ( 0.01291313371729436651, 0.01525081363757299809, 0.01758849355785162966 ),
 .UNSPECIFIED. ) ;
#820=CARTESIAN_POINT ( 'NONE',  ( -4.680456609903809628, -6.535341423376096692, -0.01688885742794853789 ) ) ;
#838=VERTEX_POINT ( 'NONE', #4441 ) ;
#844=VECTOR ( 'NONE', #6637, 1000.000000000000000 ) ;
#851=ORIENTED_EDGE ( 'NONE', *, *, #7934, .F. ) ;
#868=CARTESIAN_POINT ( 'NONE',  ( -5.690023276062290414, -5.952467836904619780, -8.269346954796052529 ) ) ;
#901=CARTESIAN_POINT ( 'NONE',  ( -6.686525924292996415, 5.377136764700138016, -0.3167204509599222950 ) ) ;
#907=ADVANCED_FACE ( 'NONE', ( #3404 ), #5334, .T. ) ;
#913=ORIENTED_EDGE ( 'NONE', *, *, #1158, .T. ) ;
#916=EDGE_CURVE ( 'NONE', #8164, #6788, #3099, .T. ) ;
#925=CARTESIAN_POINT ( 'NONE',  ( -5.080504117408890075, -2.106769544347818712, -8.400000000000018119 ) ) ;
#951=CARTESIAN_POINT ( 'NONE',  ( -3.999999999999781508, -6.928203230275875590, -8.400000000000018119 ) ) ;
#955=CARTESIAN_POINT ( 'NONE',  ( 3.319543390096007407, -7.321065037175497281, -0.01688885742779770716 ) ) ;
#960=B_SPLINE_CURVE_WITH_KNOTS ( 'NONE', 3,
 ( #5535, #4347, #4912, #5583, #7489, #247 ),
 .UNSPECIFIED., .F., .F.,
 ( 4, 2, 4 ),
 ( 0.008240550023493567466, 0.01057684187039396699, 0.01291313371729436651 ),
 .UNSPECIFIED. ) ;
#987=CARTESIAN_POINT ( 'NONE',  ( -6.661338147750939243E-13, -9.237604307034352757, -0.7145311798163467287 ) ) ;
#996=ORIENTED_EDGE ( 'NONE', *, *, #6739, .T. ) ;
#1036=B_SPLINE_CURVE_WITH_KNOTS ( 'NONE', 3,
 ( #7295, #1327, #3983, #5385, #808, #2239 ),
 .UNSPECIFIED., .F., .F.,
 ( 4, 2, 4 ),
 ( 2.380731626893816357E-07, 0.002336973833157379027, 0.004673709593152068111 ),
 .UNSPECIFIED. ) ;
#1049=AXIS2_PLACEMENT_3D ( 'NONE', #568, #2008, #5866 ) ;
#1054=CARTESIAN_POINT ( 'NONE',  ( 7.999999999999563016, -4.618802153517398423, -8.400000000000018119 ) ) ;
#1060=ORIENTED_EDGE ( 'NONE', *, *, #5786, .F. ) ;
#1082=EDGE_LOOP ( 'NONE', ( #5118, #7351, #210 ) ) ;
#1094=CARTESIAN_POINT ( 'NONE',  ( 0.000000000000000000, 0.000000000000000000, -8.400000000000018119 ) ) ;
#1109=DIRECTION ( 'NONE',  ( -0.5000000000000033307, -0.8660254037844367092, 0.000000000000000000 ) ) ;
#1141=AXIS2_PLACEMENT_3D ( 'NONE', #4803, #4838, #2838 ) ;
#1142=CARTESIAN_POINT ( 'NONE',  ( 5.080504117408890075, 2.106769544347818268, 5.551115123125782702E-14 ) ) ;
#1148=EDGE_CURVE ( 'NONE', #7803, #3139, #2994, .T. ) ;
#1158=EDGE_CURVE ( 'NONE', #799, #2305, #2606, .T. ) ;
#1165=CARTESIAN_POINT ( 'NONE',  ( 3.318518101602791148, 7.321656987762752422, 1.179340913121107448E-13 ) ) ;
#1208=AXIS2_PLACEMENT_3D ( 'NONE', #2292, #4757, #7404 ) ;
#1210=CARTESIAN_POINT ( 'NONE',  ( -3.999999999999781508, -6.928203230275875590, -8.400000000000018119 ) ) ;
#1213=ORIENTED_EDGE ( 'NONE', *, *, #1949, .T. ) ;
#1218=CARTESIAN_POINT ( 'NONE',  ( -8.000000000000229150, 4.618802153516954334, -8.400000000000018119 ) ) ;
#1220=CARTESIAN_POINT ( 'NONE',  ( -0.6543471694416780338, -8.859816792613822045, -7.903584543331102275 ) ) ;
#1228=CARTESIAN_POINT ( 'NONE',  ( 1.313474075707028232, 8.479269695850733868, -8.083279549040270240 ) ) ;
#1234=CARTESIAN_POINT ( 'NONE',  ( 2.644994884458959916, -7.710515798486509809, -8.317753204360252894 ) ) ;
#1240=ORIENTED_EDGE ( 'NONE', *, *, #1158, .F. ) ;
#1245=CARTESIAN_POINT ( 'NONE',  ( -8.000000000000222045, -3.867591403079432055, -0.4976753153247615580 ) ) ;
#1250=CIRCLE ( 'NONE', #4040, 8.000000000000007105 ) ;
#1251=VERTEX_POINT ( 'NONE', #3437 ) ;
#1256=ORIENTED_EDGE ( 'NONE', *, *, #8260, .T. ) ;
#1259=CARTESIAN_POINT ( 'NONE',  ( -8.000000000000007105, -4.618802153517398423, -7.685468820183672278 ) ) ;
#1265=( LENGTH_UNIT ( ) NAMED_UNIT ( * ) SI_UNIT ( .MILLI., .METRE. ) );
#1278=CIRCLE ( 'NONE', #4344, 5.500000000000024869 ) ;
#1295=CARTESIAN_POINT ( 'NONE',  ( 7.345652830558382362, -4.996589667937645807, -0.4964154566687026815 ) ) ;
#1311=CARTESIAN_POINT ( 'NONE',  ( -2.309976723937750887, 7.903938623646893369, -0.1306530452038467960 ) ) ;
#1314=LINE ( 'NONE', #1218, #3212 ) ;
#1327=CARTESIAN_POINT ( 'NONE',  ( 7.345652830558381474, -4.996589667937645807, -7.903584543331313661 ) ) ;
#1329=CARTESIAN_POINT ( 'NONE',  ( 0.6527133886625517967, -8.860760056386085992, -7.903039949738097647 ) ) ;
#1335=ORIENTED_EDGE ( 'NONE', *, *, #5812, .F. ) ;
#1343=CARTESIAN_POINT ( 'NONE',  ( -1.310872448938078083, 8.480771745766464420, -8.082649155111319317 ) ) ;
#1348=DIRECTION ( 'NONE',  ( 1.000000000000000000, 8.881784197001244435E-16, 0.000000000000000000 ) ) ;
#1368=DIRECTION ( 'NONE',  ( 0.000000000000000000, 0.000000000000000000, -1.000000000000000000 ) ) ;
#1380=CONICAL_SURFACE ( 'NONE', #2905, 8.000000000000007105, 1.047197551196597631 ) ;
#1401=CONICAL_SURFACE ( 'NONE', #4987, 8.000000000000007105, 1.047197551196597631 ) ;
#1408=ORIENTED_EDGE ( 'NONE', *, *, #5686, .T. ) ;
#1419=CARTESIAN_POINT ( 'NONE',  ( -6.661338147750939243E-13, -9.237604307034352757, -7.685468820183672278 ) ) ;
#1433=CARTESIAN_POINT ( 'NONE',  ( 0.000000000000000000, 0.000000000000000000, 0.000000000000000000 ) ) ;
#1437=CARTESIAN_POINT ( 'NONE',  ( 0.000000000000000000, 0.000000000000000000, 0.000000000000000000 ) ) ;
#1439=AXIS2_PLACEMENT_3D ( 'NONE', #7332, #1368, #7944 ) ;
#1446=ADVANCED_FACE ( 'NONE', ( #338 ), #3433, .T. ) ;
#1469=CARTESIAN_POINT ( 'NONE',  ( 0.000000000000000000, 0.000000000000000000, -8.400000000000018119 ) ) ;
#1470=CARTESIAN_POINT ( 'NONE',  ( -5.355005115540762084, -6.145890662065133903, -0.08224679563987397080 ) ) ;
#1476=ORIENTED_EDGE ( 'NONE', *, *, #1148, .F. ) ;
#1479=CARTESIAN_POINT ( 'NONE',  ( -1.313474075707539823, -8.479269695851096245, -0.3167204509600090589 ) ) ;
#1481=CARTESIAN_POINT ( 'NONE',  ( 8.000000000000229150, -4.440892098500626162E-13, 0.000000000000000000 ) ) ;
#1482=AXIS2_PLACEMENT_3D ( 'NONE', #2591, #7996, #3985 ) ;
#1485=ORIENTED_EDGE ( 'NONE', *, *, #5280, .F. ) ;
#1507=B_SPLINE_CURVE_WITH_KNOTS ( 'NONE', 3,
 ( #7211, #6100, #722, #4733, #4031, #3377 ),
 .UNSPECIFIED., .F., .F.,
 ( 4, 2, 4 ),
 ( 0.01291313371729436651, 0.01525081363757299462, 0.01758849355785162272 ),
 .UNSPECIFIED. ) ;
#1561=CIRCLE ( 'NONE', #1141, 5.500000000000024869 ) ;
#1585=DIRECTION ( 'NONE',  ( -0.000000000000000000, -0.000000000000000000, 1.000000000000000000 ) ) ;
#1593=PRODUCT_DEFINITION_CONTEXT ( 'detailed design', #6520, 'design' ) ;
#1601=CARTESIAN_POINT ( 'NONE',  ( 2.309976723937412491, -7.903938623647039918, -0.1306530452038728585 ) ) ;
#1606=EDGE_LOOP ( 'NONE', ( #6094, #8152, #5756 ) ) ;
#1612=ORIENTED_EDGE ( 'NONE', *, *, #7834, .T. ) ;
#1623=CARTESIAN_POINT ( 'NONE',  ( 3.999999999999559464, 6.928203230274987412, 0.000000000000000000 ) ) ;
#1637=ADVANCED_FACE ( 'NONE', ( #1763 ), #3117, .T. ) ;
#1644=EDGE_CURVE ( 'NONE', #8164, #4082, #7498, .T. ) ;
#1657=ADVANCED_FACE ( 'NONE', ( #2684, #5929 ), #5343, .F. ) ;
#1713=ADVANCED_FACE ( 'NONE', ( #8549 ), #6372, .T. ) ;
#1715=CARTESIAN_POINT ( 'NONE',  ( 4.680456609903819398, 6.535341423375429670, -8.383111142572381880 ) ) ;
#1728=CARTESIAN_POINT ( 'NONE',  ( 0.000000000000000000, 9.237604307034130713, -0.7145311798163467287 ) ) ;
#1760=VECTOR ( 'NONE', #641, 1000.000000000000000 ) ;
#1763=FACE_OUTER_BOUND ( 'NONE', #4103, .T. ) ;
#1792=VECTOR ( 'NONE', #8077, 1000.000000000000000 ) ;
#1795=VERTEX_POINT ( 'NONE', #190 ) ;
#1807=CARTESIAN_POINT ( 'NONE',  ( -6.661338147750939243E-13, -9.237604307034462892, -8.400000000000018119 ) ) ;
#1808=EDGE_CURVE ( 'NONE', #5265, #7559, #6096, .T. ) ;
#1830=DIRECTION ( 'NONE',  ( 0.000000000000000000, 0.000000000000000000, -1.000000000000000000 ) ) ;
#1855=VERTEX_POINT ( 'NONE', #810 ) ;
#1873=DIRECTION ( 'NONE',  ( -0.9237280213470678847, -0.3830490080632384942, 0.000000000000000000 ) ) ;
#1891=CARTESIAN_POINT ( 'NONE',  ( 2.309976723937405829, -7.903938623647046136, -8.269346954796146676 ) ) ;
#1896=ADVANCED_FACE ( 'NONE', ( #7474 ), #3599, .T. ) ;
#1910=ORIENTED_EDGE ( 'NONE', *, *, #5829, .F. ) ;
#1932=CARTESIAN_POINT ( 'NONE',  ( 8.000000000000007105, 4.618802153516732290, -8.400000000000018119 ) ) ;
#1942=SHAPE_REPRESENTATION ( 'hex nut style 1_am_B18.2.4.1M - Hex nut, Style 1,  M10 x 1.5, with 16mm WAF --D-N', ( #7563 ), #4502 ) ;
#1949=EDGE_CURVE ( 'NONE', #2390, #3139, #7384, .T. ) ;
#1950=CARTESIAN_POINT ( 'NONE',  ( 7.999999999999563016, -4.618802153517398423, -0.7145311798163467287 ) ) ;
#1951=AXIS2_PLACEMENT_3D ( 'NONE', #1437, #6842, #3482 ) ;
#1958=CARTESIAN_POINT ( 'NONE',  ( 0.000000000000000000, 0.000000000000000000, 5.551115123125782702E-14 ) ) ;
#1959=ORIENTED_EDGE ( 'NONE', *, *, #6846, .F. ) ;
#1969=ADVANCED_BREP_SHAPE_REPRESENTATION ( '', ( #5834, #7563 ), #4502 ) ;
#1972=SHAPE_REPRESENTATION_RELATIONSHIP ( 'NONE' , 'NONE' ,  #1942, #1969 ) ;
#1989=VERTEX_POINT ( 'NONE', #6387 ) ;
#1998=CARTESIAN_POINT ( 'NONE',  ( -7.345652830558973889, 4.996589667937345602, -7.903584543331135137 ) ) ;
#2008=DIRECTION ( 'NONE',  ( 0.000000000000000000, 0.000000000000000000, 1.000000000000000000 ) ) ;
#2020=VERTEX_POINT ( 'NONE', #7802 ) ;
#2022=ORIENTED_EDGE ( 'NONE', *, *, #1949, .F. ) ;
#2024=VECTOR ( 'NONE', #345, 1000.000000000000000 ) ;
#2039=CARTESIAN_POINT ( 'NONE',  ( 0.000000000000000000, 0.000000000000000000, -8.400000000000018119 ) ) ;
#2041=CARTESIAN_POINT ( 'NONE',  ( -3.319543390096230340, 7.321065037175420009, -8.383111142572211349 ) ) ;
#2042=CARTESIAN_POINT ( 'NONE',  ( -8.000000000000007105, 0.000000000000000000, -8.400000000000018119 ) ) ;
#2054=VERTEX_POINT ( 'NONE', #1142 ) ;
#2059=DIRECTION ( 'NONE',  ( 0.000000000000000000, 0.000000000000000000, 1.000000000000000000 ) ) ;
#2069=VERTEX_POINT ( 'NONE', #987 ) ;
#2073=DIRECTION ( 'NONE',  ( -1.000000000000000000, -8.881784197001244435E-16, -0.000000000000000000 ) ) ;
#2076=PLANE ( 'NONE',  #4729 ) ;
#2090=CARTESIAN_POINT ( 'NONE',  ( -2.644994884459265005, 7.710515798486376582, -8.317753204360265329 ) ) ;
#2144=CARTESIAN_POINT ( 'NONE',  ( 0.000000000000000000, 0.000000000000000000, -8.400000000000018119 ) ) ;
#2181=ORIENTED_EDGE ( 'NONE', *, *, #4908, .T. ) ;
#2191=EDGE_CURVE ( 'NONE', #2020, #6788, #2382, .T. ) ;
#2207=EDGE_LOOP ( 'NONE', ( #549, #5563, #8384 ) ) ;
#2234=ORIENTED_EDGE ( 'NONE', *, *, #1808, .T. ) ;
#2236=CARTESIAN_POINT ( 'NONE',  ( -4.000000000000003553, 6.928203230275209457, -8.400000000000018119 ) ) ;
#2239=CARTESIAN_POINT ( 'NONE',  ( 4.000000000000003553, -6.928203230275542523, -8.400000000000018119 ) ) ;
#2246=ADVANCED_FACE ( 'NONE', ( #2348 ), #1401, .T. ) ;
#2258=CARTESIAN_POINT ( 'NONE',  ( 2.644994884458967910, -7.710515798486506256, -0.08224679563976267094 ) ) ;
#2266=ORIENTED_EDGE ( 'NONE', *, *, #7511, .F. ) ;
#2268=ORIENTED_EDGE ( 'NONE', *, *, #8323, .T. ) ;
#2281=FACE_OUTER_BOUND ( 'NONE', #8118, .T. ) ;
#2287=CARTESIAN_POINT ( 'NONE',  ( 8.000000000000007105, 4.618802153516732290, -0.7145311798163467287 ) ) ;
#2292=CARTESIAN_POINT ( 'NONE',  ( 0.000000000000000000, 0.000000000000000000, 5.551115123125782702E-14 ) ) ;
#2299=B_SPLINE_CURVE_WITH_KNOTS ( 'NONE', 3,
 ( #2042, #4704, #4046, #6706, #735, #6070 ),
 .UNSPECIFIED., .F., .F.,
 ( 4, 2, 4 ),
 ( 0.01291313371729494418, 0.01525081363757336758, 0.01758849355785178925 ),
 .UNSPECIFIED. ) ;
#2305=VERTEX_POINT ( 'NONE', #5824 ) ;
#2311=FACE_OUTER_BOUND ( 'NONE', #3636, .T. ) ;
#2337=CARTESIAN_POINT ( 'NONE',  ( 4.000000000000003553, -6.928203230275542523, 0.000000000000000000 ) ) ;
#2348=FACE_OUTER_BOUND ( 'NONE', #8086, .T. ) ;
#2382=B_SPLINE_CURVE_WITH_KNOTS ( 'NONE', 3,
 ( #8244, #4718, #7418, #6213, #4185, #7371 ),
 .UNSPECIFIED., .F., .F.,
 ( 4, 2, 4 ),
 ( 0.008240550023493572671, 0.01057684187039396873, 0.01291313371729436651 ),
 .UNSPECIFIED. ) ;
#2390=VERTEX_POINT ( 'NONE', #5066 ) ;
#2401=EDGE_CURVE ( 'NONE', #1795, #799, #2584, .T. ) ;
#2422=CARTESIAN_POINT ( 'NONE',  ( -3.999999999999781508, -6.928203230275875590, 0.000000000000000000 ) ) ;
#2432=DIRECTION ( 'NONE',  ( -1.000000000000000000, -8.881784197001244435E-16, 0.000000000000000000 ) ) ;
#2433=DIRECTION ( 'NONE',  ( 0.000000000000000000, 0.000000000000000000, -1.000000000000000000 ) ) ;
#2435=ORIENTED_EDGE ( 'NONE', *, *, #3681, .F. ) ;
#2457=PLANE ( 'NONE',  #6567 ) ;
#2464=EDGE_LOOP ( 'NONE', ( #435, #913, #7619, #4674, #7990, #405 ) ) ;
#2473=CARTESIAN_POINT ( 'NONE',  ( 0.000000000000000000, 0.000000000000000000, -8.400000000000018119 ) ) ;
#2480=DIRECTION ( 'NONE',  ( -1.000000000000000000, -8.881784197001244435E-16, 0.000000000000000000 ) ) ;
#2502=EDGE_LOOP ( 'NONE', ( #3415, #555, #4557, #3705, #4800, #2435 ) ) ;
#2503=CARTESIAN_POINT ( 'NONE',  ( -8.000000000000007105, -4.618802153517398423, -7.685468820183672278 ) ) ;
#2505=MECHANICAL_DESIGN_GEOMETRIC_PRESENTATION_REPRESENTATION('',(#3893),#6833);
#2508=DIRECTION ( 'NONE',  ( 0.000000000000000000, 0.000000000000000000, -1.000000000000000000 ) ) ;
#2532=EDGE_LOOP ( 'NONE', ( #996, #1240, #8282 ) ) ;
#2534=DIRECTION ( 'NONE',  ( 0.000000000000000000, 0.000000000000000000, 1.000000000000000000 ) ) ;
#2540=ORIENTED_EDGE ( 'NONE', *, *, #6020, .T. ) ;
#2541=LINE ( 'NONE', #1932, #844 ) ;
#2551=FACE_OUTER_BOUND ( 'NONE', #4187, .T. ) ;
#2570=EDGE_CURVE ( 'NONE', #5906, #7803, #5731, .T. ) ;
#2578=CARTESIAN_POINT ( 'NONE',  ( -6.661338147750939243E-13, -9.237604307034352757, -7.685468820183672278 ) ) ;
#2584=LINE ( 'NONE', #6545, #1792 ) ;
#2591=CARTESIAN_POINT ( 'NONE',  ( 0.000000000000000000, 0.000000000000000000, 0.000000000000000000 ) ) ;
#2604=DIRECTION ( 'NONE',  ( -1.000000000000000000, -8.881784197001244435E-16, 0.000000000000000000 ) ) ;
#2606=B_SPLINE_CURVE_WITH_KNOTS ( 'NONE', 3,
 ( #1728, #553, #7826, #5081, #1165, #5852 ),
 .UNSPECIFIED., .F., .F.,
 ( 4, 2, 4 ),
 ( 2.380731630324309322E-07, 0.002336973833157509998, 0.004673709593151987446 ),
 .UNSPECIFIED. ) ;
#2655=CYLINDRICAL_SURFACE ( 'NONE', #57, 5.500000000000024869 ) ;
#2659=EDGE_LOOP ( 'NONE', ( #8344, #7426 ) ) ;
#2682=AXIS2_PLACEMENT_3D ( 'NONE', #6317, #4985, #8431 ) ;
#2684=FACE_BOUND ( 'NONE', #3726, .T. ) ;
#2685=CARTESIAN_POINT ( 'NONE',  ( -8.000000000000227374, 3.115336682266928836, -0.3193931313916110737 ) ) ;
#2709=CARTESIAN_POINT ( 'NONE',  ( -8.000000000000007105, 0.000000000000000000, -8.400000000000018119 ) ) ;
#2727=CARTESIAN_POINT ( 'NONE',  ( 5.080504117408896292, 2.106769544347820933, -8.400999999999992696 ) ) ;
#2750=CARTESIAN_POINT ( 'NONE',  ( -8.000000000000225597, -0.7805016046291537446, -8.399999999999890221 ) ) ;
#2751=CARTESIAN_POINT ( 'NONE',  ( 0.000000000000000000, 0.000000000000000000, -8.400000000000018119 ) ) ;
#2764=ADVANCED_FACE ( 'NONE', ( #4093 ), #7655, .T. ) ;
#2779=EDGE_CURVE ( 'NONE', #1989, #5906, #5006, .T. ) ;
#2782=DIRECTION ( 'NONE',  ( -0.9237280213470678847, -0.3830490080632384942, 0.000000000000000000 ) ) ;
#2786=CARTESIAN_POINT ( 'NONE',  ( -2.645508037661986389, -7.710219529346967526, -0.06809871960565012927 ) ) ;
#2812=ORIENTED_EDGE ( 'NONE', *, *, #2779, .T. ) ;
#2838=DIRECTION ( 'NONE',  ( 0.9237280213470678847, 0.3830490080632384942, 0.000000000000000000 ) ) ;
#2857=CARTESIAN_POINT ( 'NONE',  ( 4.339467034330982464, 6.732211846623266105, 1.328238011475783811E-13 ) ) ;
#2904=CARTESIAN_POINT ( 'NONE',  ( -8.000000000000007105, -4.618802153517398423, -7.685468820183672278 ) ) ;
#2905=AXIS2_PLACEMENT_3D ( 'NONE', #1433, #4045, #2604 ) ;
#2912=EDGE_CURVE ( 'NONE', #1989, #2069, #3630, .T. ) ;
#2939=CARTESIAN_POINT ( 'NONE',  ( 7.347286611336957485, 4.995646404165022147, -0.4969600502616601245 ) ) ;
#2964=CONICAL_SURFACE ( 'NONE', #1439, 8.000000000000007105, 1.047197551196597631 ) ;
#2993=ADVANCED_FACE ( 'NONE', ( #773 ), #5144, .T. ) ;
#2994=CIRCLE ( 'NONE', #6770, 8.000000000000007105 ) ;
#3042=CARTESIAN_POINT ( 'NONE',  ( 0.000000000000000000, 0.000000000000000000, 0.000000000000000000 ) ) ;
#3055=ORIENTED_EDGE ( 'NONE', *, *, #5043, .T. ) ;
#3071=ORIENTED_EDGE ( 'NONE', *, *, #2570, .F. ) ;
#3087=DIRECTION ( 'NONE',  ( -0.000000000000000000, -0.000000000000000000, 1.000000000000000000 ) ) ;
#3092=VECTOR ( 'NONE', #5383, 1000.000000000000000 ) ;
#3099=CIRCLE ( 'NONE', #4222, 8.000000000000007105 ) ;
#3117=PLANE ( 'NONE',  #5090 ) ;
#3118=PRODUCT_DEFINITION ( 'UNKNOWN', '', #4508, #1593 ) ;
#3137=FACE_OUTER_BOUND ( 'NONE', #7878, .T. ) ;
#3139=VERTEX_POINT ( 'NONE', #6667 ) ;
#3146=EDGE_CURVE ( 'NONE', #3833, #2054, #1278, .T. ) ;
#3161=CARTESIAN_POINT ( 'NONE',  ( -8.000000000000007105, -4.618802153517398423, -0.7145311798163467287 ) ) ;
#3212=VECTOR ( 'NONE', #4535, 1000.000000000000000 ) ;
#3219=DIRECTION ( 'NONE',  ( 0.000000000000000000, 0.000000000000000000, 1.000000000000000000 ) ) ;
#3254=EDGE_CURVE ( 'NONE', #1251, #5411, #7780, .T. ) ;
#3268=ORIENTED_EDGE ( 'NONE', *, *, #6617, .F. ) ;
#3270=FACE_OUTER_BOUND ( 'NONE', #8065, .T. ) ;
#3272=EDGE_CURVE ( 'NONE', #2069, #5906, #6962, .T. ) ;
#3344=CARTESIAN_POINT ( 'NONE',  ( -2.309976723937749110, 7.903938623646892481, -8.269346954796169769 ) ) ;
#3353=CARTESIAN_POINT ( 'NONE',  ( 8.000000000000008882, 1.572549600175327855, -0.06894455525510422012 ) ) ;
#3357=ORIENTED_EDGE ( 'NONE', *, *, #4058, .F. ) ;
#3374=CARTESIAN_POINT ( 'NONE',  ( -8.000000000000229150, 4.618802153516954334, -0.7145311798163467287 ) ) ;
#3377=CARTESIAN_POINT ( 'NONE',  ( 8.000000000000007105, 4.618802153516732290, -7.685468820183672278 ) ) ;
#3402=CARTESIAN_POINT ( 'NONE',  ( -3.319543390096229452, 7.321065037175419121, -0.01688885742780804958 ) ) ;
#3403=CARTESIAN_POINT ( 'NONE',  ( 8.000000000000012434, 0.7809653281572527250, 1.900487823754473040E-14 ) ) ;
#3404=FACE_OUTER_BOUND ( 'NONE', #1082, .T. ) ;
#3410=EDGE_CURVE ( 'NONE', #1795, #1251, #6138, .T. ) ;
#3414=DIRECTION ( 'NONE',  ( 0.000000000000000000, 0.000000000000000000, 1.000000000000000000 ) ) ;
#3415=ORIENTED_EDGE ( 'NONE', *, *, #5482, .T. ) ;
#3433=CONICAL_SURFACE ( 'NONE', #4539, 8.000000000000007105, 1.047197551196597631 ) ;
#3434=UNCERTAINTY_MEASURE_WITH_UNIT (LENGTH_MEASURE( 1.000000000000000082E-05 ), #1265, 'distance_accuracy_value', 'NONE');
#3437=CARTESIAN_POINT ( 'NONE',  ( 3.999999999999559464, 6.928203230274987412, -8.400000000000018119 ) ) ;
#3466=CARTESIAN_POINT ( 'NONE',  ( 8.000000000000007105, 4.618802153516732290, -8.400000000000018119 ) ) ;
#3476=AXIS2_PLACEMENT_3D ( 'NONE', #5700, #1830, #497 ) ;
#3482=DIRECTION ( 'NONE',  ( -1.000000000000000000, -8.881784197001244435E-16, 0.000000000000000000 ) ) ;
#3492=EDGE_LOOP ( 'NONE', ( #2266, #4191, #6871, #1910, #3901, #1335 ) ) ;
#3512=DIRECTION ( 'NONE',  ( 1.000000000000000000, 0.000000000000000000, 0.000000000000000000 ) ) ;
#3513=ORIENTED_EDGE ( 'NONE', *, *, #4938, .T. ) ;
#3518=AXIS2_PLACEMENT_3D ( 'NONE', #5869, #2534, #5826 ) ;
#3519=DIRECTION ( 'NONE',  ( 0.000000000000000000, 0.000000000000000000, -1.000000000000000000 ) ) ;
#3521=CARTESIAN_POINT ( 'NONE',  ( -6.689127551061946342, -5.375634714785059387, -8.082649155111232275 ) ) ;
#3530=ADVANCED_FACE ( 'NONE', ( #674 ), #2964, .T. ) ;
#3555=CARTESIAN_POINT ( 'NONE',  ( -5.354491962338311595, 6.146186931204400850, -0.06809871960549450376 ) ) ;
#3562=ORIENTED_EDGE ( 'NONE', *, *, #452, .T. ) ;
#3570=EDGE_CURVE ( 'NONE', #569, #2054, #6052, .T. ) ;
#3595=ORIENTED_EDGE ( 'NONE', *, *, #3834, .F. ) ;
#3599=PLANE ( 'NONE',  #6502 ) ;
#3612=ORIENTED_EDGE ( 'NONE', *, *, #8260, .F. ) ;
#3614=CARTESIAN_POINT ( 'NONE',  ( 1.310872448937630219, -8.480771745766674030, -0.3173508448887735200 ) ) ;
#3630=B_SPLINE_CURVE_WITH_KNOTS ( 'NONE', 3,
 ( #2337, #7618, #955, #2258, #1601, #3614, #6285, #294 ),
 .UNSPECIFIED., .F., .F.,
 ( 4, 2, 2, 4 ),
 ( 0.004673709593152060304, 0.005837709341827596564, 0.007001709090503132824, 0.009329708587854201873 ),
 .UNSPECIFIED. ) ;
#3636=EDGE_LOOP ( 'NONE', ( #6804, #1213, #3562, #612, #1959, #3612 ) ) ;
#3664=AXIS2_PLACEMENT_3D ( 'NONE', #6997, #3723, #8532 ) ;
#3667=ORIENTED_EDGE ( 'NONE', *, *, #2570, .T. ) ;
#3670=ADVANCED_FACE ( 'NONE', ( #3270 ), #3797, .F. ) ;
#3672=DIRECTION ( 'NONE',  ( -0.8660254037844362651, -0.5000000000000039968, 0.000000000000000000 ) ) ;
#3681=EDGE_CURVE ( 'NONE', #4082, #5338, #7875, .T. ) ;
#3694=CARTESIAN_POINT ( 'NONE',  ( -8.000000000000007105, -4.618802153517398423, -0.7145311798163467287 ) ) ;
#3698=PLANE ( 'NONE',  #5029 ) ;
#3705=ORIENTED_EDGE ( 'NONE', *, *, #5133, .F. ) ;
#3722=CIRCLE ( 'NONE', #1208, 5.500000000000024869 ) ;
#3723=DIRECTION ( 'NONE',  ( 0.000000000000000000, 0.000000000000000000, 1.000000000000000000 ) ) ;
#3726=EDGE_LOOP ( 'NONE', ( #5056, #6947 ) ) ;
#3729=CARTESIAN_POINT ( 'NONE',  ( 8.000000000000007105, 4.618802153516732290, -7.685468820183672278 ) ) ;
#3734=EDGE_CURVE ( 'NONE', #4558, #569, #1561, .T. ) ;
#3741=ORIENTED_EDGE ( 'NONE', *, *, #1148, .T. ) ;
#3773=DIRECTION ( 'NONE',  ( 0.8660254037844367092, -0.5000000000000033307, 0.000000000000000000 ) ) ;
#3777=CARTESIAN_POINT ( 'NONE',  ( 0.000000000000000000, 0.000000000000000000, 0.000000000000000000 ) ) ;
#3792=EDGE_CURVE ( 'NONE', #5906, #5923, #610, .T. ) ;
#3797=CYLINDRICAL_SURFACE ( 'NONE', #3518, 5.500000000000024869 ) ;
#3811=FACE_OUTER_BOUND ( 'NONE', #2502, .T. ) ;
#3821=ORIENTED_EDGE ( 'NONE', *, *, #916, .T. ) ;
#3826=ADVANCED_FACE ( 'NONE', ( #3811 ), #2457, .T. ) ;
#3833=VERTEX_POINT ( 'NONE', #7766 ) ;
#3834=EDGE_CURVE ( 'NONE', #8292, #1989, #5465, .T. ) ;
#3846=ORIENTED_EDGE ( 'NONE', *, *, #2912, .T. ) ;
#3865=DIRECTION ( 'NONE',  ( 0.9237280213470678847, 0.3830490080632384942, 0.000000000000000000 ) ) ;
#3876=CARTESIAN_POINT ( 'NONE',  ( -1.313474075707541822, -8.479269695851096245, -8.083279549040014444 ) ) ;
#3893=STYLED_ITEM('',(#8670),#5834);
#3901=ORIENTED_EDGE ( 'NONE', *, *, #916, .F. ) ;
#3907=DIRECTION ( 'NONE',  ( -1.000000000000000000, -8.881784197001244435E-16, 0.000000000000000000 ) ) ;
#3934=CARTESIAN_POINT ( 'NONE',  ( 0.000000000000000000, 9.237604307034130713, -7.685468820183672278 ) ) ;
#3960=CARTESIAN_POINT ( 'NONE',  ( -8.000000000000229150, 4.618802153516954334, -7.685468820183672278 ) ) ;
#3961=ORIENTED_EDGE ( 'NONE', *, *, #7230, .T. ) ;
#3978=ORIENTED_EDGE ( 'NONE', *, *, #5829, .T. ) ;
#3983=CARTESIAN_POINT ( 'NONE',  ( 6.686525924292488376, -5.377136764700389371, -8.083279549040231160 ) ) ;
#3985=DIRECTION ( 'NONE',  ( -1.000000000000000000, -8.881784197001244435E-16, 0.000000000000000000 ) ) ;
#3986=CARTESIAN_POINT ( 'NONE',  ( -8.000000000000007105, 0.000000000000000000, 0.000000000000000000 ) ) ;
#3987=CARTESIAN_POINT ( 'NONE',  ( 0.000000000000000000, 9.237604307034130713, -8.400000000000018119 ) ) ;
#3995=CARTESIAN_POINT ( 'NONE',  ( 5.354491962337974975, -6.146186931204550064, -0.06809871960543639746 ) ) ;
#4000=DIRECTION ( 'NONE',  ( 0.000000000000000000, 0.000000000000000000, 1.000000000000000000 ) ) ;
#4005=CARTESIAN_POINT ( 'NONE',  ( -2.644994884459267226, 7.710515798486376582, -0.08224679563975054175 ) ) ;
#4031=CARTESIAN_POINT ( 'NONE',  ( 8.000000000000008882, 3.871967595401863083, -7.901061386767627148 ) ) ;
#4033=VERTEX_POINT ( 'NONE', #2503 ) ;
#4040=AXIS2_PLACEMENT_3D ( 'NONE', #2039, #7347, #7872 ) ;
#4045=DIRECTION ( 'NONE',  ( 0.000000000000000000, 0.000000000000000000, -1.000000000000000000 ) ) ;
#4046=CARTESIAN_POINT ( 'NONE',  ( -8.000000000000225597, 1.572549600175543905, -8.331055444744766447 ) ) ;
#4058=EDGE_CURVE ( 'NONE', #2020, #8164, #1036, .T. ) ;
#4061=AXIS2_PLACEMENT_3D ( 'NONE', #4323, #6987, #3672 ) ;
#4064=ORIENTED_EDGE ( 'NONE', *, *, #6739, .F. ) ;
#4066=( NAMED_UNIT ( * ) PLANE_ANGLE_UNIT ( ) SI_UNIT ( $, .RADIAN. ) );
#4074=DIRECTION ( 'NONE',  ( 0.000000000000000000, 0.000000000000000000, -1.000000000000000000 ) ) ;
#4082=VERTEX_POINT ( 'NONE', #1419 ) ;
#4093=FACE_OUTER_BOUND ( 'NONE', #2207, .T. ) ;
#4103=EDGE_LOOP ( 'NONE', ( #6344, #6429, #3846, #7003, #8196, #3357 ) ) ;
#4159=CARTESIAN_POINT ( 'NONE',  ( 5.355005115540778959, 6.145890662064466881, -0.08224679563958640915 ) ) ;
#4185=CARTESIAN_POINT ( 'NONE',  ( 8.000000000000012434, -0.7805016046295530918, -8.399999999999987921 ) ) ;
#4186=ADVANCED_FACE ( 'NONE', ( #2281 ), #6576, .T. ) ;
#4187=EDGE_LOOP ( 'NONE', ( #4641, #3268, #7831, #3961, #1612, #7918 ) ) ;
#4191=ORIENTED_EDGE ( 'NONE', *, *, #1808, .F. ) ;
#4197=CARTESIAN_POINT ( 'NONE',  ( -8.000000000000229150, 4.618802153516954334, -0.7145311798163467287 ) ) ;
#4203=CARTESIAN_POINT ( 'NONE',  ( 0.000000000000000000, 0.000000000000000000, 0.000000000000000000 ) ) ;
#4212=CARTESIAN_POINT ( 'NONE',  ( 0.000000000000000000, 0.000000000000000000, 0.000000000000000000 ) ) ;
#4222=AXIS2_PLACEMENT_3D ( 'NONE', #2751, #5409, #7405 ) ;
#4251=CARTESIAN_POINT ( 'NONE',  ( 5.690023276062296631, 5.952467836903953646, -0.1306530452036860357 ) ) ;
#4316=CIRCLE ( 'NONE', #5431, 5.500000000000024869 ) ;
#4318=VERTEX_POINT ( 'NONE', #6668 ) ;
#4323=CARTESIAN_POINT ( 'NONE',  ( 0.000000000000000000, 9.237604307034130713, -8.400000000000018119 ) ) ;
#4344=AXIS2_PLACEMENT_3D ( 'NONE', #1958, #3219, #1873 ) ;
#4347=CARTESIAN_POINT ( 'NONE',  ( 8.000000000000015987, -3.867591403079598589, -0.4976753153247004402 ) ) ;
#4383=CARTESIAN_POINT ( 'NONE',  ( 5.355005115540780736, 6.145890662064464216, -8.317753204360434083 ) ) ;
#4384=PRODUCT_DEFINITION_SHAPE ( 'NONE', 'NONE',  #3118 ) ;
#4402=DIRECTION ( 'NONE',  ( 0.000000000000000000, 0.000000000000000000, -1.000000000000000000 ) ) ;
#4441=CARTESIAN_POINT ( 'NONE',  ( -8.000000000000229150, 4.618802153516954334, -7.685468820183672278 ) ) ;
#4442=VECTOR ( 'NONE', #5972, 1000.000000000000000 ) ;
#4458=ORIENTED_EDGE ( 'NONE', *, *, #8274, .T. ) ;
#4464=DIRECTION ( 'NONE',  ( 0.5000000000000029976, -0.8660254037844370423, 0.000000000000000000 ) ) ;
#4502=( GEOMETRIC_REPRESENTATION_CONTEXT ( 3 ) GLOBAL_UNCERTAINTY_ASSIGNED_CONTEXT ( ( #8559 ) ) GLOBAL_UNIT_ASSIGNED_CONTEXT ( ( #7989, #4066, #5922 ) ) REPRESENTATION_CONTEXT ( 'NONE', 'WORKASPACE' ) );
#4508=PRODUCT_DEFINITION_FORMATION_WITH_SPECIFIED_SOURCE ( 'ANY', '', #8343, .NOT_KNOWN. ) ;
#4535=DIRECTION ( 'NONE',  ( 0.000000000000000000, 0.000000000000000000, 1.000000000000000000 ) ) ;
#4539=AXIS2_PLACEMENT_3D ( 'NONE', #4212, #3519, #5673 ) ;
#4557=ORIENTED_EDGE ( 'NONE', *, *, #3792, .T. ) ;
#4558=VERTEX_POINT ( 'NONE', #925 ) ;
#4609=ORIENTED_EDGE ( 'NONE', *, *, #3570, .T. ) ;
#4611=CARTESIAN_POINT ( 'NONE',  ( -8.000000000000007105, 0.000000000000000000, 0.000000000000000000 ) ) ;
#4615=CARTESIAN_POINT ( 'NONE',  ( -0.6527133886630747117, 8.860760056385830197, -7.903039949738215775 ) ) ;
#4638=B_SPLINE_CURVE_WITH_KNOTS ( 'NONE', 3,
 ( #5979, #734, #2041, #2090, #3344, #1343, #4615, #5263 ),
 .UNSPECIFIED., .F., .F.,
 ( 4, 2, 2, 4 ),
 ( 0.004673709593152869553, 0.005837709341828217595, 0.007001709090503566504, 0.009329708587854264323 ),
 .UNSPECIFIED. ) ;
#4641=ORIENTED_EDGE ( 'NONE', *, *, #8323, .F. ) ;
#4656=CARTESIAN_POINT ( 'NONE',  ( -5.080504117408896292, -2.106769544347821377, -8.400999999999992696 ) ) ;
#4664=ORIENTED_EDGE ( 'NONE', *, *, #3734, .F. ) ;
#4669=AXIS2_PLACEMENT_3D ( 'NONE', #7144, #4402, #7062 ) ;
#4674=ORIENTED_EDGE ( 'NONE', *, *, #7834, .F. ) ;
#4704=CARTESIAN_POINT ( 'NONE',  ( -8.000000000000225597, 0.7809653281575846817, -8.399999999999884892 ) ) ;
#4705=EDGE_LOOP ( 'NONE', ( #8238, #4664, #3055, #8474 ) ) ;
#4718=CARTESIAN_POINT ( 'NONE',  ( 8.000000000000015987, -3.867591403079595480, -7.902324684675320121 ) ) ;
#4729=AXIS2_PLACEMENT_3D ( 'NONE', #3987, #680, #192 ) ;
#4733=CARTESIAN_POINT ( 'NONE',  ( 8.000000000000008882, 3.115336682266736101, -8.080606868608565918 ) ) ;
#4757=DIRECTION ( 'NONE',  ( 0.000000000000000000, 0.000000000000000000, 1.000000000000000000 ) ) ;
#4791=CARTESIAN_POINT ( 'NONE',  ( -5.354491962338311595, 6.146186931204400850, -8.331901280394522047 ) ) ;
#4795=CARTESIAN_POINT ( 'NONE',  ( 7.347286611336957485, 4.995646404165020371, -7.903039949738357883 ) ) ;
#4800=ORIENTED_EDGE ( 'NONE', *, *, #7084, .F. ) ;
#4803=CARTESIAN_POINT ( 'NONE',  ( 0.000000000000000000, 0.000000000000000000, -8.400000000000018119 ) ) ;
#4838=DIRECTION ( 'NONE',  ( -0.000000000000000000, -0.000000000000000000, 1.000000000000000000 ) ) ;
#4857=EDGE_CURVE ( 'NONE', #4033, #7559, #401, .T. ) ;
#4870=DIRECTION ( 'NONE',  ( -0.000000000000000000, -0.000000000000000000, 1.000000000000000000 ) ) ;
#4908=EDGE_CURVE ( 'NONE', #2054, #3833, #3722, .T. ) ;
#4912=CARTESIAN_POINT ( 'NONE',  ( 8.000000000000015987, -3.098204225878660623, -0.3157906771919842814 ) ) ;
#4921=DIRECTION ( 'NONE',  ( 0.000000000000000000, 0.000000000000000000, 1.000000000000000000 ) ) ;
#4938=EDGE_CURVE ( 'NONE', #8292, #4318, #815, .T. ) ;
#4950=B_SPLINE_CURVE_WITH_KNOTS ( 'NONE', 3,
 ( #1950, #1295, #7305, #3995, #6658, #7515 ),
 .UNSPECIFIED., .F., .F.,
 ( 4, 2, 4 ),
 ( 2.380731626811020739E-07, 0.002336973833157370787, 0.004673709593152060304 ),
 .UNSPECIFIED. ) ;
#4967=PLANE ( 'NONE',  #4061 ) ;
#4985=DIRECTION ( 'NONE',  ( 0.000000000000000000, 0.000000000000000000, -1.000000000000000000 ) ) ;
#4987=AXIS2_PLACEMENT_3D ( 'NONE', #1094, #5092, #7064 ) ;
#5006=CIRCLE ( 'NONE', #1951, 8.000000000000007105 ) ;
#5029=AXIS2_PLACEMENT_3D ( 'NONE', #6363, #8394, #387 ) ;
#5043=EDGE_CURVE ( 'NONE', #4558, #3833, #5895, .T. ) ;
#5048=CARTESIAN_POINT ( 'NONE',  ( 8.000000000000007105, 4.618802153516732290, -7.685468820183672278 ) ) ;
#5056=ORIENTED_EDGE ( 'NONE', *, *, #3146, .F. ) ;
#5066=CARTESIAN_POINT ( 'NONE',  ( -8.000000000000229150, 4.618802153516954334, -0.7145311798163467287 ) ) ;
#5081=CARTESIAN_POINT ( 'NONE',  ( 2.645508037661675083, 7.710219529346487910, -0.06809871960532241919 ) ) ;
#5090=AXIS2_PLACEMENT_3D ( 'NONE', #1807, #4464, #7126 ) ;
#5092=DIRECTION ( 'NONE',  ( 0.000000000000000000, 0.000000000000000000, 1.000000000000000000 ) ) ;
#5108=CARTESIAN_POINT ( 'NONE',  ( -7.347286611336937945, -4.995646404165699828, -0.4969600502618697346 ) ) ;
#5118=ORIENTED_EDGE ( 'NONE', *, *, #6846, .T. ) ;
#5131=DIRECTION ( 'NONE',  ( 0.000000000000000000, 0.000000000000000000, 1.000000000000000000 ) ) ;
#5133=EDGE_CURVE ( 'NONE', #4033, #5923, #6516, .T. ) ;
#5135=CARTESIAN_POINT ( 'NONE',  ( -3.999999999999781508, -6.928203230275875590, -8.400000000000018119 ) ) ;
#5143=B_SPLINE_CURVE_WITH_KNOTS ( 'NONE', 3,
 ( #3986, #55, #7337, #2685, #5344, #3374 ),
 .UNSPECIFIED., .F., .F.,
 ( 4, 2, 4 ),
 ( 0.01291313371729494071, 0.01525081363757336758, 0.01758849355785179619 ),
 .UNSPECIFIED. ) ;
#5144=CONICAL_SURFACE ( 'NONE', #6287, 8.000000000000007105, 1.047197551196597631 ) ;
#5148=ORIENTED_EDGE ( 'NONE', *, *, #2191, .F. ) ;
#5187=CARTESIAN_POINT ( 'NONE',  ( -2.645508037661987277, -7.710219529346969303, -8.331901280394371057 ) ) ;
#5262=ORIENTED_EDGE ( 'NONE', *, *, #6020, .F. ) ;
#5263=CARTESIAN_POINT ( 'NONE',  ( 0.000000000000000000, 9.237604307034130713, -7.685468820183672278 ) ) ;
#5265=VERTEX_POINT ( 'NONE', #2236 ) ;
#5280=EDGE_CURVE ( 'NONE', #569, #4558, #4316, .T. ) ;
#5282=AXIS2_PLACEMENT_3D ( 'NONE', #2144, #4000, #1348 ) ;
#5320=DIRECTION ( 'NONE',  ( 0.000000000000000000, 0.000000000000000000, 1.000000000000000000 ) ) ;
#5329=AXIS2_PLACEMENT_3D ( 'NONE', #8450, #2480, #5131 ) ;
#5334=CONICAL_SURFACE ( 'NONE', #7976, 8.000000000000007105, 1.047197551196597631 ) ;
#5338=VERTEX_POINT ( 'NONE', #1210 ) ;
#5343=PLANE ( 'NONE',  #6485 ) ;
#5344=CARTESIAN_POINT ( 'NONE',  ( -8.000000000000229150, 3.871967595402047824, -0.4989386132325554501 ) ) ;
#5346=FACE_OUTER_BOUND ( 'NONE', #3492, .T. ) ;
#5357=CARTESIAN_POINT ( 'NONE',  ( -4.681481898397175989, 6.534749472788146107, -8.399999999999964828 ) ) ;
#5361=ORIENTED_EDGE ( 'NONE', *, *, #3272, .F. ) ;
#5383=DIRECTION ( 'NONE',  ( 0.000000000000000000, 0.000000000000000000, 1.000000000000000000 ) ) ;
#5385=CARTESIAN_POINT ( 'NONE',  ( 5.354491962337973199, -6.146186931204551840, -8.331901280394582443 ) ) ;
#5409=DIRECTION ( 'NONE',  ( -0.000000000000000000, -0.000000000000000000, 1.000000000000000000 ) ) ;
#5411=VERTEX_POINT ( 'NONE', #5048 ) ;
#5416=ADVANCED_FACE ( 'NONE', ( #7707 ), #205, .T. ) ;
#5429=CLOSED_SHELL ( 'NONE', ( #3670, #6234, #1896, #362, #1637, #3826, #6365, #1657, #7398, #4186, #907, #2246, #2993, #2764, #62, #5416, #1446, #3530, #6927, #1713, #5917, #8240 ) ) ;
#5431=AXIS2_PLACEMENT_3D ( 'NONE', #2473, #3087, #3865 ) ;
#5453=ORIENTED_EDGE ( 'NONE', *, *, #5686, .F. ) ;
#5454=CARTESIAN_POINT ( 'NONE',  ( -3.999999999999781508, -6.928203230275875590, 0.000000000000000000 ) ) ;
#5465=CIRCLE ( 'NONE', #2682, 8.000000000000007105 ) ;
#5482=EDGE_CURVE ( 'NONE', #4082, #2069, #475, .T. ) ;
#5516=ORIENTED_EDGE ( 'NONE', *, *, #8274, .F. ) ;
#5534=CARTESIAN_POINT ( 'NONE',  ( -4.339467034331054407, -6.732211846623885165, -8.399999999999826272 ) ) ;
#5535=CARTESIAN_POINT ( 'NONE',  ( 7.999999999999563016, -4.618802153517398423, -0.7145311798163467287 ) ) ;
#5548=( NAMED_UNIT ( * ) PLANE_ANGLE_UNIT ( ) SI_UNIT ( $, .RADIAN. ) );
#5561=CARTESIAN_POINT ( 'NONE',  ( -4.681481898397175989, 6.534749472788146107, -5.458788531875063334E-14 ) ) ;
#5563=ORIENTED_EDGE ( 'NONE', *, *, #3681, .T. ) ;
#5569=ORIENTED_EDGE ( 'NONE', *, *, #3834, .T. ) ;
#5583=CARTESIAN_POINT ( 'NONE',  ( 8.000000000000012434, -1.555946510856606624, -0.06708870216341396298 ) ) ;
#5605=EDGE_LOOP ( 'NONE', ( #2812, #5361, #794 ) ) ;
#5632=CARTESIAN_POINT ( 'NONE',  ( -4.680456609903821175, -6.535341423376089587, -8.383111142572069241 ) ) ;
#5673=DIRECTION ( 'NONE',  ( -1.000000000000000000, -8.881784197001244435E-16, 0.000000000000000000 ) ) ;
#5686=EDGE_CURVE ( 'NONE', #5923, #7803, #6722, .T. ) ;
#5700=CARTESIAN_POINT ( 'NONE',  ( 0.000000000000000000, 0.000000000000000000, 0.000000000000000000 ) ) ;
#5713=CARTESIAN_POINT ( 'NONE',  ( 3.999999999999559464, 6.928203230274987412, -8.400000000000018119 ) ) ;
#5731=CIRCLE ( 'NONE', #3476, 8.000000000000007105 ) ;
#5756=ORIENTED_EDGE ( 'NONE', *, *, #7511, .T. ) ;
#5786=EDGE_CURVE ( 'NONE', #1855, #1989, #4950, .T. ) ;
#5802=CARTESIAN_POINT ( 'NONE',  ( -6.689127551061941013, -5.375634714785060275, -0.3173508448887821798 ) ) ;
#5807=CARTESIAN_POINT ( 'NONE',  ( -6.661338147750939243E-13, -9.237604307034462892, -8.400000000000018119 ) ) ;
#5812=EDGE_CURVE ( 'NONE', #5338, #8164, #1250, .T. ) ;
#5824=CARTESIAN_POINT ( 'NONE',  ( 3.999999999999559464, 6.928203230274987412, 0.000000000000000000 ) ) ;
#5826=DIRECTION ( 'NONE',  ( -0.9237280213470678847, -0.3830490080632384942, 0.000000000000000000 ) ) ;
#5829=EDGE_CURVE ( 'NONE', #6788, #1251, #6284, .T. ) ;
#5834=MANIFOLD_SOLID_BREP ( 'EndChamfer', #5429 ) ;
#5839=CARTESIAN_POINT ( 'NONE',  ( -8.000000000000007105, -4.618802153517398423, -8.400000000000018119 ) ) ;
#5852=CARTESIAN_POINT ( 'NONE',  ( 3.999999999999559464, 6.928203230274987412, 0.000000000000000000 ) ) ;
#5866=DIRECTION ( 'NONE',  ( 1.000000000000000000, 8.881784197001244435E-16, 0.000000000000000000 ) ) ;
#5869=CARTESIAN_POINT ( 'NONE',  ( 0.000000000000000000, 0.000000000000000000, -8.400999999999992696 ) ) ;
#5885=CARTESIAN_POINT ( 'NONE',  ( 0.000000000000000000, 9.237604307034130713, 0.000000000000000000 ) ) ;
#5895=LINE ( 'NONE', #4656, #1760 ) ;
#5906=VERTEX_POINT ( 'NONE', #2422 ) ;
#5917=ADVANCED_FACE ( 'NONE', ( #7085 ), #8376, .T. ) ;
#5922=( NAMED_UNIT ( * ) SI_UNIT ( $, .STERADIAN. ) SOLID_ANGLE_UNIT ( ) );
#5923=VERTEX_POINT ( 'NONE', #3161 ) ;
#5929=FACE_OUTER_BOUND ( 'NONE', #7205, .T. ) ;
#5950=CARTESIAN_POINT ( 'NONE',  ( -3.660532965669041516, 7.124194613927598674, -4.381983780462242249E-14 ) ) ;
#5956=ORIENTED_EDGE ( 'NONE', *, *, #7467, .F. ) ;
#5964=CARTESIAN_POINT ( 'NONE',  ( 3.660532965668862992, -7.124194613927656405, -8.399999999999993250 ) ) ;
#5972=DIRECTION ( 'NONE',  ( 0.000000000000000000, 0.000000000000000000, 1.000000000000000000 ) ) ;
#5979=CARTESIAN_POINT ( 'NONE',  ( -4.000000000000003553, 6.928203230275209457, -8.400000000000018119 ) ) ;
#5988=APPLICATION_CONTEXT ( 'automotive_design' ) ;
#5999=AXIS2_PLACEMENT_3D ( 'NONE', #756, #3414, #7548 ) ;
#6020=EDGE_CURVE ( 'NONE', #7803, #2390, #5143, .T. ) ;
#6031=CARTESIAN_POINT ( 'NONE',  ( -1.310872448938079859, 8.480771745766464420, -0.3173508448886962485 ) ) ;
#6052=LINE ( 'NONE', #2727, #3092 ) ;
#6070=CARTESIAN_POINT ( 'NONE',  ( -8.000000000000229150, 4.618802153516954334, -7.685468820183672278 ) ) ;
#6073=B_SPLINE_CURVE_WITH_KNOTS ( 'NONE', 3,
 ( #7275, #5950, #3402, #4005, #1311, #6031, #28, #7621 ),
 .UNSPECIFIED., .F., .F.,
 ( 4, 2, 2, 4 ),
 ( 0.004673709593152869553, 0.005837709341828219330, 0.007001709090503569974, 0.009329708587854271262 ),
 .UNSPECIFIED. ) ;
#6094=ORIENTED_EDGE ( 'NONE', *, *, #7084, .T. ) ;
#6096=CIRCLE ( 'NONE', #7481, 8.000000000000007105 ) ;
#6100=CARTESIAN_POINT ( 'NONE',  ( 8.000000000000012434, 0.7809653281572520589, -8.400000000000034106 ) ) ;
#6104=DIRECTION ( 'NONE',  ( 0.000000000000000000, 0.000000000000000000, 1.000000000000000000 ) ) ;
#6106=CARTESIAN_POINT ( 'NONE',  ( 5.080504117408890075, 2.106769544347818268, -8.400000000000018119 ) ) ;
#6138=B_SPLINE_CURVE_WITH_KNOTS ( 'NONE', 3,
 ( #3934, #582, #1228, #6428, #7899, #503 ),
 .UNSPECIFIED., .F., .F.,
 ( 4, 2, 4 ),
 ( 2.380731630400558434E-07, 0.002336973833157513902, 0.004673709593151988313 ),
 .UNSPECIFIED. ) ;
#6154=CARTESIAN_POINT ( 'NONE',  ( 0.000000000000000000, 0.000000000000000000, -8.400999999999992696 ) ) ;
#6158=CARTESIAN_POINT ( 'NONE',  ( -3.318518101603001647, -7.321656987763291546, -2.234845609353635682E-13 ) ) ;
#6196=CARTESIAN_POINT ( 'NONE',  ( -7.347286611336940609, -4.995646404165698939, -7.903039949738148273 ) ) ;
#6213=CARTESIAN_POINT ( 'NONE',  ( 8.000000000000012434, -1.555946510856605292, -8.332911297836602671 ) ) ;
#6223=CARTESIAN_POINT ( 'NONE',  ( 0.000000000000000000, 0.000000000000000000, -8.400000000000018119 ) ) ;
#6234=ADVANCED_FACE ( 'NONE', ( #2311 ), #4967, .T. ) ;
#6263=DIRECTION ( 'NONE',  ( -0.8660254037844365982, 0.5000000000000035527, -0.000000000000000000 ) ) ;
#6265=CARTESIAN_POINT ( 'NONE',  ( 6.689127551061961441, 5.375634714784386148, -0.3173508448885462019 ) ) ;
#6284=CIRCLE ( 'NONE', #280, 8.000000000000007105 ) ;
#6285=CARTESIAN_POINT ( 'NONE',  ( 0.6527133886625527959, -8.860760056386080663, -0.4969600502619245797 ) ) ;
#6287=AXIS2_PLACEMENT_3D ( 'NONE', #1469, #6104, #101 ) ;
#6310=DIRECTION ( 'NONE',  ( -0.000000000000000000, -0.000000000000000000, 1.000000000000000000 ) ) ;
#6317=CARTESIAN_POINT ( 'NONE',  ( 0.000000000000000000, 0.000000000000000000, 0.000000000000000000 ) ) ;
#6344=ORIENTED_EDGE ( 'NONE', *, *, #6617, .T. ) ;
#6363=CARTESIAN_POINT ( 'NONE',  ( 8.000000000000007105, 4.618802153516732290, -8.400000000000018119 ) ) ;
#6365=ADVANCED_FACE ( 'NONE', ( #3137 ), #6488, .T. ) ;
#6371=DIRECTION ( 'NONE',  ( 0.000000000000000000, 0.000000000000000000, -1.000000000000000000 ) ) ;
#6372=CONICAL_SURFACE ( 'NONE', #1482, 8.000000000000007105, 1.047197551196597631 ) ;
#6387=CARTESIAN_POINT ( 'NONE',  ( 4.000000000000003553, -6.928203230275542523, 0.000000000000000000 ) ) ;
#6392=CARTESIAN_POINT ( 'NONE',  ( 5.690023276062294855, 5.952467836903953646, -8.269346954796333193 ) ) ;
#6408=CARTESIAN_POINT ( 'NONE',  ( 8.000000000000229150, -4.440892098500626162E-13, -8.400000000000018119 ) ) ;
#6428=CARTESIAN_POINT ( 'NONE',  ( 2.645508037661670642, 7.710219529346487910, -8.331901280394694354 ) ) ;
#6429=ORIENTED_EDGE ( 'NONE', *, *, #5786, .T. ) ;
#6485=AXIS2_PLACEMENT_3D ( 'NONE', #5885, #4074, #2073 ) ;
#6488=PLANE ( 'NONE',  #5329 ) ;
#6502=AXIS2_PLACEMENT_3D ( 'NONE', #3466, #93, #6263 ) ;
#6516=LINE ( 'NONE', #6610, #4442 ) ;
#6520=APPLICATION_CONTEXT ( 'automotive_design' ) ;
#6545=CARTESIAN_POINT ( 'NONE',  ( 0.000000000000000000, 9.237604307034130713, -8.400000000000018119 ) ) ;
#6562=CARTESIAN_POINT ( 'NONE',  ( -8.000000000000222045, -3.098204225878420814, -0.3157906771920435673 ) ) ;
#6567=AXIS2_PLACEMENT_3D ( 'NONE', #5839, #1109, #3773 ) ;
#6576=CONICAL_SURFACE ( 'NONE', #3664, 8.000000000000007105, 1.047197551196597631 ) ;
#6600=CARTESIAN_POINT ( 'NONE',  ( 3.319543390095996749, -7.321065037175506163, -8.383111142572218455 ) ) ;
#6610=CARTESIAN_POINT ( 'NONE',  ( -8.000000000000007105, -4.618802153517398423, -8.400000000000018119 ) ) ;
#6617=EDGE_CURVE ( 'NONE', #2020, #1855, #7623, .T. ) ;
#6637=DIRECTION ( 'NONE',  ( 0.000000000000000000, 0.000000000000000000, 1.000000000000000000 ) ) ;
#6646=CARTESIAN_POINT ( 'NONE',  ( 1.310872448937626222, -8.480771745766677583, -8.082649155111246486 ) ) ;
#6658=CARTESIAN_POINT ( 'NONE',  ( 4.681481898396925523, -6.534749472788247360, -2.235319947804098595E-14 ) ) ;
#6667=CARTESIAN_POINT ( 'NONE',  ( -4.000000000000003553, 6.928203230275209457, 0.000000000000000000 ) ) ;
#6668=CARTESIAN_POINT ( 'NONE',  ( 8.000000000000007105, 4.618802153516732290, -0.7145311798163467287 ) ) ;
#6671=B_SPLINE_CURVE_WITH_KNOTS ( 'NONE', 3,
 ( #3960, #1998, #649, #4791, #5357, #6758 ),
 .UNSPECIFIED., .F., .F.,
 ( 4, 2, 4 ),
 ( 2.380731634175168328E-07, 0.002336973833158143606, 0.004673709593152869553 ),
 .UNSPECIFIED. ) ;
#6680=CIRCLE ( 'NONE', #5999, 8.000000000000007105 ) ;
#6706=CARTESIAN_POINT ( 'NONE',  ( -8.000000000000227374, 3.115336682266930168, -8.080606868608406046 ) ) ;
#6722=B_SPLINE_CURVE_WITH_KNOTS ( 'NONE', 3,
 ( #7218, #1245, #6562, #601, #8561, #4611 ),
 .UNSPECIFIED., .F., .F.,
 ( 4, 2, 4 ),
 ( 0.008240550023493499812, 0.01057684187039422026, 0.01291313371729494071 ),
 .UNSPECIFIED. ) ;
#6739=EDGE_CURVE ( 'NONE', #3139, #2305, #531, .T. ) ;
#6758=CARTESIAN_POINT ( 'NONE',  ( -4.000000000000003553, 6.928203230275209457, -8.400000000000018119 ) ) ;
#6766=CARTESIAN_POINT ( 'NONE',  ( 8.000000000000008882, 3.115336682266734325, -0.3193931313914511461 ) ) ;
#6770=AXIS2_PLACEMENT_3D ( 'NONE', #3042, #6371, #2432 ) ;
#6788=VERTEX_POINT ( 'NONE', #6408 ) ;
#6804=ORIENTED_EDGE ( 'NONE', *, *, #80, .T. ) ;
#6833=( GEOMETRIC_REPRESENTATION_CONTEXT ( 3 ) GLOBAL_UNCERTAINTY_ASSIGNED_CONTEXT ( ( #3434 ) ) GLOBAL_UNIT_ASSIGNED_CONTEXT ( ( #1265, #5548, #7813 ) ) REPRESENTATION_CONTEXT ( 'NONE', 'WORKASPACE' ) );
#6839=CARTESIAN_POINT ( 'NONE',  ( -5.355005115540773630, -6.145890662065128573, -8.317753204360139208 ) ) ;
#6842=DIRECTION ( 'NONE',  ( 0.000000000000000000, 0.000000000000000000, -1.000000000000000000 ) ) ;
#6846=EDGE_CURVE ( 'NONE', #5265, #1795, #4638, .T. ) ;
#6870=CARTESIAN_POINT ( 'NONE',  ( -7.345652830558973889, 4.996589667937345602, -0.4964154566688861459 ) ) ;
#6871=ORIENTED_EDGE ( 'NONE', *, *, #6998, .F. ) ;
#6911=DIRECTION ( 'NONE',  ( -1.000000000000000000, -6.217248937900875838E-15, 0.000000000000000000 ) ) ;
#6926=CARTESIAN_POINT ( 'NONE',  ( 0.000000000000000000, 0.000000000000000000, -8.400000000000018119 ) ) ;
#6927=ADVANCED_FACE ( 'NONE', ( #648 ), #1380, .T. ) ;
#6947=ORIENTED_EDGE ( 'NONE', *, *, #4908, .F. ) ;
#6955=DIRECTION ( 'NONE',  ( -1.000000000000000000, -8.881784197001244435E-16, 0.000000000000000000 ) ) ;
#6962=B_SPLINE_CURVE_WITH_KNOTS ( 'NONE', 3,
 ( #118, #7535, #1479, #2786, #6158, #5454 ),
 .UNSPECIFIED., .F., .F.,
 ( 4, 2, 4 ),
 ( 2.380731628247750877E-07, 0.002336973833157300531, 0.004673709593151774075 ),
 .UNSPECIFIED. ) ;
#6964=CARTESIAN_POINT ( 'NONE',  ( 8.000000000000008882, 3.871967595401859974, -0.4989386132323923584 ) ) ;
#6987=DIRECTION ( 'NONE',  ( -0.5000000000000041078, 0.8660254037844363761, 0.000000000000000000 ) ) ;
#6992=SHAPE_DEFINITION_REPRESENTATION ( #4384, #1942 ) ;
#6997=CARTESIAN_POINT ( 'NONE',  ( 0.000000000000000000, 0.000000000000000000, -8.400000000000018119 ) ) ;
#6998=EDGE_CURVE ( 'NONE', #1251, #5265, #7627, .T. ) ;
#7003=ORIENTED_EDGE ( 'NONE', *, *, #5482, .F. ) ;
#7041=CARTESIAN_POINT ( 'NONE',  ( 6.689127551061957000, 5.375634714784386148, -8.082649155111475636 ) ) ;
#7062=DIRECTION ( 'NONE',  ( -1.000000000000000000, -8.881784197001244435E-16, 0.000000000000000000 ) ) ;
#7064=DIRECTION ( 'NONE',  ( 1.000000000000000000, 8.881784197001244435E-16, 0.000000000000000000 ) ) ;
#7084=EDGE_CURVE ( 'NONE', #5338, #4033, #8266, .T. ) ;
#7085=FACE_OUTER_BOUND ( 'NONE', #7397, .T. ) ;
#7116=CARTESIAN_POINT ( 'NONE',  ( -4.000000000000003553, 6.928203230275209457, 0.000000000000000000 ) ) ;
#7126=DIRECTION ( 'NONE',  ( 0.8660254037844369313, 0.5000000000000028866, 0.000000000000000000 ) ) ;
#7131=EDGE_LOOP ( 'NONE', ( #7353, #3821, #5148 ) ) ;
#7144=CARTESIAN_POINT ( 'NONE',  ( 0.000000000000000000, 0.000000000000000000, 0.000000000000000000 ) ) ;
#7183=CARTESIAN_POINT ( 'NONE',  ( 0.000000000000000000, 0.000000000000000000, 0.000000000000000000 ) ) ;
#7205=EDGE_LOOP ( 'NONE', ( #1476, #3071, #7372, #3595, #596, #4064 ) ) ;
#7211=CARTESIAN_POINT ( 'NONE',  ( 8.000000000000229150, -4.440892098500626162E-13, -8.400000000000018119 ) ) ;
#7218=CARTESIAN_POINT ( 'NONE',  ( -8.000000000000007105, -4.618802153517398423, -0.7145311798163467287 ) ) ;
#7220=CARTESIAN_POINT ( 'NONE',  ( 0.000000000000000000, 0.000000000000000000, -8.400000000000018119 ) ) ;
#7225=ORIENTED_EDGE ( 'NONE', *, *, #5133, .T. ) ;
#7230=EDGE_CURVE ( 'NONE', #6788, #5411, #1507, .T. ) ;
#7235=FACE_OUTER_BOUND ( 'NONE', #1606, .T. ) ;
#7275=CARTESIAN_POINT ( 'NONE',  ( -4.000000000000003553, 6.928203230275209457, 0.000000000000000000 ) ) ;
#7295=CARTESIAN_POINT ( 'NONE',  ( 7.999999999999563016, -4.618802153517398423, -7.685468820183672278 ) ) ;
#7305=CARTESIAN_POINT ( 'NONE',  ( 6.686525924292487488, -5.377136764700389371, -0.3167204509597881246 ) ) ;
#7332=CARTESIAN_POINT ( 'NONE',  ( 0.000000000000000000, 0.000000000000000000, 0.000000000000000000 ) ) ;
#7336=CARTESIAN_POINT ( 'NONE',  ( 4.000000000000003553, -6.928203230275542523, -8.400000000000018119 ) ) ;
#7337=CARTESIAN_POINT ( 'NONE',  ( -8.000000000000225597, 1.572549600175544349, -0.06894455525525224060 ) ) ;
#7347=DIRECTION ( 'NONE',  ( -0.000000000000000000, -0.000000000000000000, 1.000000000000000000 ) ) ;
#7351=ORIENTED_EDGE ( 'NONE', *, *, #3410, .T. ) ;
#7353=ORIENTED_EDGE ( 'NONE', *, *, #4058, .T. ) ;
#7357=CARTESIAN_POINT ( 'NONE',  ( 8.000000000000007105, 4.618802153516732290, -0.7145311798163467287 ) ) ;
#7371=CARTESIAN_POINT ( 'NONE',  ( 8.000000000000229150, -4.440892098500626162E-13, -8.400000000000018119 ) ) ;
#7372=ORIENTED_EDGE ( 'NONE', *, *, #2779, .F. ) ;
#7384=B_SPLINE_CURVE_WITH_KNOTS ( 'NONE', 3,
 ( #4197, #6870, #901, #3555, #5561, #7116 ),
 .UNSPECIFIED., .F., .F.,
 ( 4, 2, 4 ),
 ( 2.380731634175322118E-07, 0.002336973833158143606, 0.004673709593152869553 ),
 .UNSPECIFIED. ) ;
#7397=EDGE_LOOP ( 'NONE', ( #5262, #3741, #2022 ) ) ;
#7398=ADVANCED_FACE ( 'NONE', ( #3, #5346 ), #2076, .T. ) ;
#7400=EDGE_LOOP ( 'NONE', ( #2268, #5569, #1060 ) ) ;
#7404=DIRECTION ( 'NONE',  ( -0.9237280213470678847, -0.3830490080632384942, 0.000000000000000000 ) ) ;
#7405=DIRECTION ( 'NONE',  ( -1.000000000000000000, -8.881784197001244435E-16, 0.000000000000000000 ) ) ;
#7418=CARTESIAN_POINT ( 'NONE',  ( 8.000000000000015987, -3.098204225878657514, -8.084209322808037612 ) ) ;
#7426=ORIENTED_EDGE ( 'NONE', *, *, #5280, .T. ) ;
#7440=CARTESIAN_POINT ( 'NONE',  ( -4.339467034331056183, -6.732211846623884277, -1.918902320027780141E-13 ) ) ;
#7465=DIRECTION ( 'NONE',  ( 1.000000000000000000, 8.881784197001244435E-16, 0.000000000000000000 ) ) ;
#7467=EDGE_CURVE ( 'NONE', #2305, #4318, #705, .T. ) ;
#7474=FACE_OUTER_BOUND ( 'NONE', #2464, .T. ) ;
#7478=DIRECTION ( 'NONE',  ( 0.000000000000000000, 0.000000000000000000, 1.000000000000000000 ) ) ;
#7481=AXIS2_PLACEMENT_3D ( 'NONE', #6223, #1585, #6911 ) ;
#7489=CARTESIAN_POINT ( 'NONE',  ( 8.000000000000012434, -0.7805016046295540910, -3.176542958793075869E-14 ) ) ;
#7498=B_SPLINE_CURVE_WITH_KNOTS ( 'NONE', 3,
 ( #7336, #5964, #6600, #1234, #1891, #6646, #1329, #7948 ),
 .UNSPECIFIED., .F., .F.,
 ( 4, 2, 2, 4 ),
 ( 0.004673709593152068111, 0.005837709341827601768, 0.007001709090503135426, 0.009329708587854201873 ),
 .UNSPECIFIED. ) ;
#7511=EDGE_CURVE ( 'NONE', #7559, #5338, #274, .T. ) ;
#7515=CARTESIAN_POINT ( 'NONE',  ( 4.000000000000003553, -6.928203230275542523, 0.000000000000000000 ) ) ;
#7520=CARTESIAN_POINT ( 'NONE',  ( 0.000000000000000000, 0.000000000000000000, -8.400000000000018119 ) ) ;
#7530=DIRECTION ( 'NONE',  ( -1.000000000000000000, 7.703719777548936406E-31, 0.000000000000000000 ) ) ;
#7535=CARTESIAN_POINT ( 'NONE',  ( -0.6543471694416775897, -8.859816792613825598, -0.4964154566689172321 ) ) ;
#7548=DIRECTION ( 'NONE',  ( 1.000000000000000000, 8.881784197001244435E-16, 0.000000000000000000 ) ) ;
#7559=VERTEX_POINT ( 'NONE', #7722 ) ;
#7561=CARTESIAN_POINT ( 'NONE',  ( 4.680456609903819398, 6.535341423375429670, -0.01688885742763771361 ) ) ;
#7563=AXIS2_PLACEMENT_3D ( 'NONE', #4203, #7478, #3512 ) ;
#7566=EDGE_LOOP ( 'NONE', ( #3667, #5453, #8143 ) ) ;
#7618=CARTESIAN_POINT ( 'NONE',  ( 3.660532965668862548, -7.124194613927656405, -2.499488348229032566E-14 ) ) ;
#7619=ORIENTED_EDGE ( 'NONE', *, *, #7467, .T. ) ;
#7621=CARTESIAN_POINT ( 'NONE',  ( 0.000000000000000000, 9.237604307034130713, -0.7145311798163467287 ) ) ;
#7623=LINE ( 'NONE', #1054, #398 ) ;
#7627=CIRCLE ( 'NONE', #106, 8.000000000000007105 ) ;
#7655=CONICAL_SURFACE ( 'NONE', #5282, 8.000000000000007105, 1.047197551196597631 ) ;
#7659=CARTESIAN_POINT ( 'NONE',  ( 8.000000000000229150, -4.440892098500626162E-13, 0.000000000000000000 ) ) ;
#7687=CARTESIAN_POINT ( 'NONE',  ( 4.339467034330983353, 6.732211846623264329, -8.400000000000151346 ) ) ;
#7707=FACE_OUTER_BOUND ( 'NONE', #7566, .T. ) ;
#7722=CARTESIAN_POINT ( 'NONE',  ( -8.000000000000007105, 0.000000000000000000, -8.400000000000018119 ) ) ;
#7766=CARTESIAN_POINT ( 'NONE',  ( -5.080504117408896292, -2.106769544347821377, 5.551115123125782702E-14 ) ) ;
#7780=B_SPLINE_CURVE_WITH_KNOTS ( 'NONE', 3,
 ( #5713, #7687, #1715, #4383, #6392, #7041, #4795, #3729 ),
 .UNSPECIFIED., .F., .F.,
 ( 4, 2, 2, 4 ),
 ( 0.004673709593151988313, 0.005837709341827519369, 0.007001709090503049557, 0.009329708587854111668 ),
 .UNSPECIFIED. ) ;
#7793=CONICAL_SURFACE ( 'NONE', #1049, 8.000000000000007105, 1.047197551196597631 ) ;
#7802=CARTESIAN_POINT ( 'NONE',  ( 7.999999999999563016, -4.618802153517398423, -7.685468820183672278 ) ) ;
#7803=VERTEX_POINT ( 'NONE', #625 ) ;
#7813=( NAMED_UNIT ( * ) SI_UNIT ( $, .STERADIAN. ) SOLID_ANGLE_UNIT ( ) );
#7826=CARTESIAN_POINT ( 'NONE',  ( 1.313474075707030897, 8.479269695850733868, -0.3167204509597497664 ) ) ;
#7831=ORIENTED_EDGE ( 'NONE', *, *, #2191, .T. ) ;
#7834=EDGE_CURVE ( 'NONE', #5411, #4318, #2541, .T. ) ;
#7872=DIRECTION ( 'NONE',  ( -1.000000000000000000, -8.881784197001244435E-16, 0.000000000000000000 ) ) ;
#7875=B_SPLINE_CURVE_WITH_KNOTS ( 'NONE', 3,
 ( #2578, #1220, #3876, #5187, #8452, #5135 ),
 .UNSPECIFIED., .F., .F.,
 ( 4, 2, 4 ),
 ( 2.380731628247754583E-07, 0.002336973833157303133, 0.004673709593151780146 ),
 .UNSPECIFIED. ) ;
#7878=EDGE_LOOP ( 'NONE', ( #7225, #1408, #2540, #258, #5516, #478 ) ) ;
#7899=CARTESIAN_POINT ( 'NONE',  ( 3.318518101602789372, 7.321656987762753310, -8.400000000000137135 ) ) ;
#7918=ORIENTED_EDGE ( 'NONE', *, *, #4938, .F. ) ;
#7934=EDGE_CURVE ( 'NONE', #8292, #2305, #6680, .T. ) ;
#7944=DIRECTION ( 'NONE',  ( -1.000000000000000000, -8.881784197001244435E-16, 0.000000000000000000 ) ) ;
#7948=CARTESIAN_POINT ( 'NONE',  ( -6.661338147750939243E-13, -9.237604307034352757, -7.685468820183672278 ) ) ;
#7965=DIRECTION ( 'NONE',  ( 0.000000000000000000, 0.000000000000000000, 1.000000000000000000 ) ) ;
#7974=DIRECTION ( 'NONE',  ( 1.000000000000000000, 8.881784197001244435E-16, 0.000000000000000000 ) ) ;
#7976=AXIS2_PLACEMENT_3D ( 'NONE', #76, #5320, #7974 ) ;
#7989=( LENGTH_UNIT ( ) NAMED_UNIT ( * ) SI_UNIT ( .MILLI., .METRE. ) );
#7990=ORIENTED_EDGE ( 'NONE', *, *, #3254, .F. ) ;
#7994=ORIENTED_EDGE ( 'NONE', *, *, #7230, .F. ) ;
#7996=DIRECTION ( 'NONE',  ( 0.000000000000000000, 0.000000000000000000, -1.000000000000000000 ) ) ;
#8050=FACE_OUTER_BOUND ( 'NONE', #4705, .T. ) ;
#8059=CARTESIAN_POINT ( 'NONE',  ( -8.000000000000222045, -3.098204225878416818, -8.084209322807978992 ) ) ;
#8065=EDGE_LOOP ( 'NONE', ( #1485, #4609, #2181, #8261 ) ) ;
#8077=DIRECTION ( 'NONE',  ( 0.000000000000000000, 0.000000000000000000, 1.000000000000000000 ) ) ;
#8086=EDGE_LOOP ( 'NONE', ( #783, #7994, #3978 ) ) ;
#8118=EDGE_LOOP ( 'NONE', ( #1256, #2234, #4458 ) ) ;
#8143=ORIENTED_EDGE ( 'NONE', *, *, #3792, .F. ) ;
#8152=ORIENTED_EDGE ( 'NONE', *, *, #4857, .T. ) ;
#8164=VERTEX_POINT ( 'NONE', #67 ) ;
#8196=ORIENTED_EDGE ( 'NONE', *, *, #1644, .F. ) ;
#8238=ORIENTED_EDGE ( 'NONE', *, *, #3570, .F. ) ;
#8240=ADVANCED_FACE ( 'NONE', ( #8050 ), #2655, .F. ) ;
#8244=CARTESIAN_POINT ( 'NONE',  ( 7.999999999999563016, -4.618802153517398423, -7.685468820183672278 ) ) ;
#8260=EDGE_CURVE ( 'NONE', #838, #5265, #6671, .T. ) ;
#8261=ORIENTED_EDGE ( 'NONE', *, *, #5043, .F. ) ;
#8266=B_SPLINE_CURVE_WITH_KNOTS ( 'NONE', 3,
 ( #951, #5534, #5632, #6839, #868, #3521, #6196, #2904 ),
 .UNSPECIFIED., .F., .F.,
 ( 4, 2, 2, 4 ),
 ( 0.004673709593151780146, 0.005837709341827351968, 0.007001709090502924657, 0.009329708587854070034 ),
 .UNSPECIFIED. ) ;
#8274=EDGE_CURVE ( 'NONE', #7559, #838, #2299, .T. ) ;
#8282=ORIENTED_EDGE ( 'NONE', *, *, #452, .F. ) ;
#8292=VERTEX_POINT ( 'NONE', #7659 ) ;
#8323=EDGE_CURVE ( 'NONE', #1855, #8292, #960, .T. ) ;
#8343=PRODUCT ( 'hex nut style 1_am_B18.2.4.1M - Hex nut, Style 1,  M10 x 1.5, with 16mm WAF --D-N', 'hex nut style 1_am_B18.2.4.1M - Hex nut, Style 1,  M10 x 1.5, with 16mm WAF --D-N', '', ( #8375 ) ) ;
#8344=ORIENTED_EDGE ( 'NONE', *, *, #3734, .T. ) ;
#8375=PRODUCT_CONTEXT ( 'NONE', #5988, 'mechanical' ) ;
#8376=CONICAL_SURFACE ( 'NONE', #126, 8.000000000000007105, 1.047197551196597631 ) ;
#8384=ORIENTED_EDGE ( 'NONE', *, *, #5812, .T. ) ;
#8394=DIRECTION ( 'NONE',  ( -1.000000000000000000, -8.881784197001244435E-16, 0.000000000000000000 ) ) ;
#8431=DIRECTION ( 'NONE',  ( -1.000000000000000000, -8.881784197001244435E-16, 0.000000000000000000 ) ) ;
#8449=CARTESIAN_POINT ( 'NONE',  ( 0.000000000000000000, 9.237604307034130713, -0.7145311798163467287 ) ) ;
#8450=CARTESIAN_POINT ( 'NONE',  ( -8.000000000000229150, 4.618802153516954334, -8.400000000000018119 ) ) ;
#8452=CARTESIAN_POINT ( 'NONE',  ( -3.318518101603002535, -7.321656987763293323, -8.399999999999796074 ) ) ;
#8474=ORIENTED_EDGE ( 'NONE', *, *, #3146, .T. ) ;
#8532=DIRECTION ( 'NONE',  ( 1.000000000000000000, 8.881784197001244435E-16, 0.000000000000000000 ) ) ;
#8549=FACE_OUTER_BOUND ( 'NONE', #2532, .T. ) ;
#8559=UNCERTAINTY_MEASURE_WITH_UNIT (LENGTH_MEASURE( 1.000000000000000082E-05 ), #7989, 'distance_accuracy_value', 'NONE');
#8561=CARTESIAN_POINT ( 'NONE',  ( -8.000000000000225597, -0.7805016046291550769, -1.288946976495813912E-13 ) ) ;
#8664=COLOUR_RGB('Black',0.12,0.14,0.17);
#8665=FILL_AREA_STYLE_COLOUR('',#8664);
#8666=FILL_AREA_STYLE('',(#8665));
#8667=SURFACE_STYLE_FILL_AREA(#8666);
#8668=SURFACE_SIDE_STYLE('',(#8667));
#8669=SURFACE_STYLE_USAGE(.BOTH.,#8668);
#8670=PRESENTATION_STYLE_ASSIGNMENT((#8669));
ENDSEC;
END-ISO-10303-21;
